ISO-10303-21;
HEADER;
FILE_DESCRIPTION (('STEP AP214'),
    '1' );
FILE_NAME ('socket head cap screw_iso_ISO 4762 M5 x 20 - 20N.step',
    '2026-10-08T14:09:18',
    ( '' ),
    ( '' ),
    'SwSTEP 2.0',
    'SolidWorks 2026',
    '' );
FILE_SCHEMA (( 'AUTOMOTIVE_DESIGN' ));
ENDSEC;

DATA;
#3=EDGE_LOOP ( 'NONE', ( #3250, #4536, #2732 ) ) ;
#16=ORIENTED_EDGE ( 'NONE', *, *, #4419, .T. ) ;
#20=CARTESIAN_POINT ( 'NONE',  ( 2.500000000000000000, -1.178949249685218303, -2.041999999999998039 ) ) ;
#27=DIRECTION ( 'NONE',  ( 0.000000000000000000, -1.000000000000000000, 1.287488025362403787E-15 ) ) ;
#36=ORIENTED_EDGE ( 'NONE', *, *, #664, .F. ) ;
#40=FACE_OUTER_BOUND ( 'NONE', #1799, .T. ) ;
#44=LINE ( 'NONE', #3926, #164 ) ;
#45=VERTEX_POINT ( 'NONE', #656 ) ;
#47=ADVANCED_FACE ( 'NONE', ( #2594 ), #1860, .F. ) ;
#50=FACE_OUTER_BOUND ( 'NONE', #3870, .T. ) ;
#51=PRODUCT ( 'socket head cap screw_iso_ISO 4762 M5 x 20 - 20N', 'socket head cap screw_iso_ISO 4762 M5 x 20 - 20N', '', ( #972 ) ) ;
#52=DIRECTION ( 'NONE',  ( -1.000000000000000000, -0.000000000000000000, -0.000000000000000000 ) ) ;
#57=DIRECTION ( 'NONE',  ( 1.000000000000000000, 0.000000000000000000, 0.000000000000000000 ) ) ;
#69=ORIENTED_EDGE ( 'NONE', *, *, #2839, .T. ) ;
#70=ADVANCED_FACE ( 'NONE', ( #1108 ), #102, .F. ) ;
#71=ADVANCED_FACE ( 'NONE', ( #4306 ), #1906, .T. ) ;
#89=AXIS2_PLACEMENT_3D ( 'NONE', #3740, #316, #1588 ) ;
#90=ORIENTED_EDGE ( 'NONE', *, *, #4505, .T. ) ;
#98=ORIENTED_EDGE ( 'NONE', *, *, #3653, .F. ) ;
#102=PLANE ( 'NONE',  #3242 ) ;
#108=SHAPE_DEFINITION_REPRESENTATION ( #4246, #4748 ) ;
#115=VERTEX_POINT ( 'NONE', #877 ) ;
#120=ADVANCED_FACE ( 'NONE', ( #2037 ), #2439, .T. ) ;
#127=( NAMED_UNIT ( * ) SI_UNIT ( $, .STERADIAN. ) SOLID_ANGLE_UNIT ( ) );
#128=DIRECTION ( 'NONE',  ( 0.000000000000000000, -0.8660254037844390407, -0.4999999999999994449 ) ) ;
#138=ORIENTED_EDGE ( 'NONE', *, *, #3058, .T. ) ;
#142=DIRECTION ( 'NONE',  ( -1.000000000000000000, 0.000000000000000000, -0.000000000000000000 ) ) ;
#146=EDGE_CURVE ( 'NONE', #3852, #4296, #1281, .T. ) ;
#154=FACE_OUTER_BOUND ( 'NONE', #602, .T. ) ;
#164=VECTOR ( 'NONE', #508, 1000.000000000000000 ) ;
#172=EDGE_CURVE ( 'NONE', #645, #1989, #1795, .T. ) ;
#178=( GEOMETRIC_REPRESENTATION_CONTEXT ( 3 ) GLOBAL_UNCERTAINTY_ASSIGNED_CONTEXT ( ( #350 ) ) GLOBAL_UNIT_ASSIGNED_CONTEXT ( ( #3558, #3977, #127 ) ) REPRESENTATION_CONTEXT ( 'NONE', 'WORKASPACE' ) );
#182=CIRCLE ( 'NONE', #2505, 2.041999999999999815 ) ;
#183=VECTOR ( 'NONE', #1498, 999.9999999999998863 ) ;
#207=CARTESIAN_POINT ( 'NONE',  ( -31.74999999999995737, 0.000000000000000000, 0.000000000000000000 ) ) ;
#211=ORIENTED_EDGE ( 'NONE', *, *, #1116, .F. ) ;
#214=CARTESIAN_POINT ( 'NONE',  ( 0.2500000000000002220, 4.898587196589412829E-16, -4.000000000000000000 ) ) ;
#216=VERTEX_POINT ( 'NONE', #3805 ) ;
#219=ORIENTED_EDGE ( 'NONE', *, *, #939, .F. ) ;
#220=ADVANCED_FACE ( 'NONE', ( #382 ), #3087, .T. ) ;
#252=DIRECTION ( 'NONE',  ( 0.000000000000000000, 0.000000000000000000, -1.000000000000000000 ) ) ;
#262=ORIENTED_EDGE ( 'NONE', *, *, #2624, .F. ) ;
#274=ORIENTED_EDGE ( 'NONE', *, *, #1417, .T. ) ;
#285=DIRECTION ( 'NONE',  ( 0.000000000000000000, 0.4999999999999993339, -0.8660254037844390407 ) ) ;
#290=PLANE ( 'NONE',  #1520 ) ;
#292=ORIENTED_EDGE ( 'NONE', *, *, #1706, .F. ) ;
#304=DIRECTION ( 'NONE',  ( -1.000000000000000000, -0.000000000000000000, -0.000000000000000000 ) ) ;
#309=( NAMED_UNIT ( * ) PLANE_ANGLE_UNIT ( ) SI_UNIT ( $, .RADIAN. ) );
#315=CARTESIAN_POINT ( 'NONE',  ( 5.000000000000004441, 0.000000000000000000, 4.250000000000000000 ) ) ;
#316=DIRECTION ( 'NONE',  ( -1.000000000000000000, -0.000000000000000000, -0.000000000000000000 ) ) ;
#317=VECTOR ( 'NONE', #4957, 1000.000000000000000 ) ;
#321=PLANE ( 'NONE',  #826 ) ;
#329=LINE ( 'NONE', #4502, #575 ) ;
#330=CARTESIAN_POINT ( 'NONE',  ( -31.74999999999995737, 0.000000000000000000, 0.000000000000000000 ) ) ;
#331=EDGE_LOOP ( 'NONE', ( #1142, #2436, #2467, #3469, #3020 ) ) ;
#332=VECTOR ( 'NONE', #3365, 999.9999999999998863 ) ;
#339=AXIS2_PLACEMENT_3D ( 'NONE', #3312, #4913, #3750 ) ;
#340=VERTEX_POINT ( 'NONE', #1371 ) ;
#341=CIRCLE ( 'NONE', #1452, 2.700000000000001066 ) ;
#346=DIRECTION ( 'NONE',  ( -1.000000000000000000, -0.000000000000000000, -0.000000000000000000 ) ) ;
#348=CIRCLE ( 'NONE', #3779, 4.000000000000000000 ) ;
#350=UNCERTAINTY_MEASURE_WITH_UNIT (LENGTH_MEASURE( 1.000000000000000082E-05 ), #3558, 'distance_accuracy_value', 'NONE');
#355=ADVANCED_FACE ( 'NONE', ( #643 ), #4445, .F. ) ;
#356=EDGE_LOOP ( 'NONE', ( #4695, #2450 ) ) ;
#360=ORIENTED_EDGE ( 'NONE', *, *, #3573, .F. ) ;
#365=FACE_OUTER_BOUND ( 'NONE', #770, .T. ) ;
#382=FACE_OUTER_BOUND ( 'NONE', #4619, .T. ) ;
#387=ADVANCED_FACE ( 'NONE', ( #2250 ), #4495, .F. ) ;
#397=ORIENTED_EDGE ( 'NONE', *, *, #3827, .F. ) ;
#404=LINE ( 'NONE', #3458, #2987 ) ;
#408=DIRECTION ( 'NONE',  ( 0.000000000000000000, 0.5000000000000011102, 0.8660254037844380415 ) ) ;
#416=ORIENTED_EDGE ( 'NONE', *, *, #3654, .T. ) ;
#420=MECHANICAL_DESIGN_GEOMETRIC_PRESENTATION_REPRESENTATION('',(#1141),#178);
#424=ORIENTED_EDGE ( 'NONE', *, *, #3827, .T. ) ;
#434=ORIENTED_EDGE ( 'NONE', *, *, #1360, .F. ) ;
#447=DIRECTION ( 'NONE',  ( -1.000000000000000000, -0.000000000000000000, -0.000000000000000000 ) ) ;
#455=DIRECTION ( 'NONE',  ( 0.000000000000000000, -1.000000000000000000, 1.287488025362403787E-15 ) ) ;
#466=CARTESIAN_POINT ( 'NONE',  ( 0.000000000000000000, 1.178949249685213863, -2.042000000000001148 ) ) ;
#475=DIRECTION ( 'NONE',  ( 0.000000000000000000, 0.000000000000000000, 1.000000000000000000 ) ) ;
#477=LINE ( 'NONE', #4645, #4099 ) ;
#478=STYLED_ITEM ( 'NONE', ( #1032 ), #996 ) ;
#480=DIRECTION ( 'NONE',  ( 0.000000000000000000, 0.000000000000000000, 1.000000000000000000 ) ) ;
#481=DIRECTION ( 'NONE',  ( 0.000000000000000000, -0.5000000000000012212, -0.8660254037844380415 ) ) ;
#484=VERTEX_POINT ( 'NONE', #4908 ) ;
#494=ADVANCED_FACE ( 'NONE', ( #851 ), #1302, .F. ) ;
#508=DIRECTION ( 'NONE',  ( -1.000000000000000000, -0.000000000000000000, -0.000000000000000000 ) ) ;
#515=CARTESIAN_POINT ( 'NONE',  ( 25.00000000000000000, 0.000000000000000000, 0.000000000000000000 ) ) ;
#517=ORIENTED_EDGE ( 'NONE', *, *, #3654, .F. ) ;
#521=CARTESIAN_POINT ( 'NONE',  ( 2.500000000000000000, -1.178949249685213863, 2.042000000000002924 ) ) ;
#529=FACE_OUTER_BOUND ( 'NONE', #1640, .T. ) ;
#543=ORIENTED_EDGE ( 'NONE', *, *, #2810, .F. ) ;
#547=EDGE_CURVE ( 'NONE', #2929, #3315, #44, .T. ) ;
#564=CARTESIAN_POINT ( 'NONE',  ( 2.500000000000000000, 2.357898499370433054, -1.951563910473907981E-15 ) ) ;
#569=FACE_OUTER_BOUND ( 'NONE', #2980, .T. ) ;
#571=VERTEX_POINT ( 'NONE', #1569 ) ;
#575=VECTOR ( 'NONE', #2937, 1000.000000000000000 ) ;
#591=ORIENTED_EDGE ( 'NONE', *, *, #4411, .T. ) ;
#592=DIRECTION ( 'NONE',  ( -1.000000000000000000, -0.000000000000000000, -0.000000000000000000 ) ) ;
#602=EDGE_LOOP ( 'NONE', ( #718, #4210, #661, #1411 ) ) ;
#605=CARTESIAN_POINT ( 'NONE',  ( 24.55500000000002103, 3.061616997868384620E-16, -2.500000000000001332 ) ) ;
#606=ORIENTED_EDGE ( 'NONE', *, *, #4600, .T. ) ;
#608=DIRECTION ( 'NONE',  ( 0.000000000000000000, 0.000000000000000000, 1.000000000000000000 ) ) ;
#609=APPLICATION_CONTEXT ( 'automotive_design' ) ;
#616=ORIENTED_EDGE ( 'NONE', *, *, #3305, .T. ) ;
#621=ORIENTED_EDGE ( 'NONE', *, *, #2351, .F. ) ;
#629=CARTESIAN_POINT ( 'NONE',  ( 2.500000000000000000, 2.357898499370433054, -1.951563910473907981E-15 ) ) ;
#641=CIRCLE ( 'NONE', #2418, 4.250000000000000000 ) ;
#643=FACE_OUTER_BOUND ( 'NONE', #3434, .T. ) ;
#644=AXIS2_PLACEMENT_3D ( 'NONE', #1689, #4751, #1713 ) ;
#645=VERTEX_POINT ( 'NONE', #1974 ) ;
#655=EDGE_CURVE ( 'NONE', #2974, #2709, #2729, .T. ) ;
#656=CARTESIAN_POINT ( 'NONE',  ( 2.500000000000000000, -2.357898499370432610, 3.252606517456513302E-15 ) ) ;
#657=CONICAL_SURFACE ( 'NONE', #3947, 2.055000000000000160, 0.7853981633974721488 ) ;
#661=ORIENTED_EDGE ( 'NONE', *, *, #3804, .T. ) ;
#664=EDGE_CURVE ( 'NONE', #1044, #571, #3133, .T. ) ;
#669=DIRECTION ( 'NONE',  ( 0.000000000000000000, 0.000000000000000000, 1.000000000000000000 ) ) ;
#681=SURFACE_STYLE_FILL_AREA ( #2969 ) ;
#682=CARTESIAN_POINT ( 'NONE',  ( 25.00000000000000000, 0.000000000000000000, 0.000000000000000000 ) ) ;
#700=CARTESIAN_POINT ( 'NONE',  ( 2.500000000000000000, 0.000000000000000000, 0.000000000000000000 ) ) ;
#706=ORIENTED_EDGE ( 'NONE', *, *, #4609, .F. ) ;
#716=DIRECTION ( 'NONE',  ( 0.000000000000000000, -0.5000000000000011102, -0.8660254037844379305 ) ) ;
#718=ORIENTED_EDGE ( 'NONE', *, *, #4825, .T. ) ;
#735=EDGE_LOOP ( 'NONE', ( #2699, #2041, #219, #517, #2538 ) ) ;
#736=EDGE_LOOP ( 'NONE', ( #292, #543, #3161, #69, #606 ) ) ;
#764=ORIENTED_EDGE ( 'NONE', *, *, #4789, .T. ) ;
#769=ORIENTED_EDGE ( 'NONE', *, *, #2998, .T. ) ;
#770=EDGE_LOOP ( 'NONE', ( #2887, #775 ) ) ;
#772=DIRECTION ( 'NONE',  ( -1.000000000000000000, -0.000000000000000000, -0.000000000000000000 ) ) ;
#773=CARTESIAN_POINT ( 'NONE',  ( 0.000000000000000000, -1.178949249685213863, 2.042000000000002924 ) ) ;
#774=CARTESIAN_POINT ( 'NONE',  ( 2.500000000000000000, 2.357898499370433054, -1.951563910473907981E-15 ) ) ;
#775=ORIENTED_EDGE ( 'NONE', *, *, #1417, .F. ) ;
#778=CARTESIAN_POINT ( 'NONE',  ( 2.500000000000000000, -1.178949249685213863, 2.042000000000002924 ) ) ;
#783=ADVANCED_FACE ( 'NONE', ( #569 ), #3598, .T. ) ;
#789=ORIENTED_EDGE ( 'NONE', *, *, #1903, .F. ) ;
#794=ORIENTED_EDGE ( 'NONE', *, *, #3305, .F. ) ;
#798=DIRECTION ( 'NONE',  ( 0.000000000000000000, 0.000000000000000000, 1.000000000000000000 ) ) ;
#804=AXIS2_PLACEMENT_3D ( 'NONE', #1991, #1195, #3919 ) ;
#813=ORIENTED_EDGE ( 'NONE', *, *, #4024, .F. ) ;
#824=CARTESIAN_POINT ( 'NONE',  ( 0.000000000000000000, 0.000000000000000000, 0.000000000000000000 ) ) ;
#826=AXIS2_PLACEMENT_3D ( 'NONE', #4881, #4295, #1197 ) ;
#829=CIRCLE ( 'NONE', #1462, 4.250000000000000000 ) ;
#830=UNCERTAINTY_MEASURE_WITH_UNIT (LENGTH_MEASURE( 1.000000000000000082E-05 ), #3517, 'distance_accuracy_value', 'NONE');
#851=FACE_OUTER_BOUND ( 'NONE', #2534, .T. ) ;
#857=LINE ( 'NONE', #3094, #4406 ) ;
#868=CARTESIAN_POINT ( 'NONE',  ( 0.000000000000000000, 0.000000000000000000, 0.000000000000000000 ) ) ;
#869=EDGE_CURVE ( 'NONE', #4351, #2929, #1287, .T. ) ;
#876=VECTOR ( 'NONE', #716, 1000.000000000000114 ) ;
#877=CARTESIAN_POINT ( 'NONE',  ( 0.000000000000000000, -1.178949249685218303, -2.041999999999998039 ) ) ;
#879=DIRECTION ( 'NONE',  ( 0.000000000000000000, -1.000000000000000000, 1.471414886128461471E-15 ) ) ;
#895=AXIS2_PLACEMENT_3D ( 'NONE', #2335, #3116, #879 ) ;
#908=PRESENTATION_STYLE_ASSIGNMENT (( #2061 ) ) ;
#909=PLANE ( 'NONE',  #2835 ) ;
#915=VECTOR ( 'NONE', #4018, 1000.000000000000000 ) ;
#939=EDGE_CURVE ( 'NONE', #1050, #216, #4903, .T. ) ;
#949=DIRECTION ( 'NONE',  ( 1.000000000000000000, 0.000000000000000000, 0.000000000000000000 ) ) ;
#970=CIRCLE ( 'NONE', #1609, 0.2000000000000000944 ) ;
#972=PRODUCT_CONTEXT ( 'NONE', #2153, 'mechanical' ) ;
#981=LINE ( 'NONE', #2853, #1772 ) ;
#986=EDGE_CURVE ( 'NONE', #3389, #2431, #4002, .T. ) ;
#996=ADVANCED_BREP_SHAPE_REPRESENTATION ( '', ( #1999, #1918 ), #3816 ) ;
#998=ADVANCED_FACE ( 'NONE', ( #4621 ), #2428, .F. ) ;
#999=ADVANCED_FACE ( 'NONE', ( #4643 ), #2652, .F. ) ;
#1014=ORIENTED_EDGE ( 'NONE', *, *, #1706, .T. ) ;
#1018=DIRECTION ( 'NONE',  ( 0.000000000000000000, 0.000000000000000000, 1.000000000000000000 ) ) ;
#1022=CARTESIAN_POINT ( 'NONE',  ( 2.500000000000000000, 2.357898499370433054, -1.951563910473907981E-15 ) ) ;
#1032=PRESENTATION_STYLE_ASSIGNMENT (( #4012 ) ) ;
#1037=CARTESIAN_POINT ( 'NONE',  ( 5.000000000000004441, 0.000000000000000000, 0.000000000000000000 ) ) ;
#1044=VERTEX_POINT ( 'NONE', #3873 ) ;
#1049=VECTOR ( 'NONE', #2565, 1000.000000000000114 ) ;
#1050=VERTEX_POINT ( 'NONE', #1565 ) ;
#1054=LINE ( 'NONE', #2535, #2256 ) ;
#1064=DIRECTION ( 'NONE',  ( 0.000000000000000000, 1.224646799147353207E-16, 1.000000000000000000 ) ) ;
#1065=ORIENTED_EDGE ( 'NONE', *, *, #1116, .T. ) ;
#1072=ORIENTED_EDGE ( 'NONE', *, *, #2379, .F. ) ;
#1073=LINE ( 'NONE', #2182, #876 ) ;
#1086=DIRECTION ( 'NONE',  ( 0.000000000000000000, 0.000000000000000000, 1.000000000000000000 ) ) ;
#1097=LINE ( 'NONE', #20, #2884 ) ;
#1101=MECHANICAL_DESIGN_GEOMETRIC_PRESENTATION_REPRESENTATION('',(#478),#1495);
#1102=DIRECTION ( 'NONE',  ( -1.000000000000000000, -0.000000000000000000, -0.000000000000000000 ) ) ;
#1103=CARTESIAN_POINT ( 'NONE',  ( 2.500000000000000000, -2.357898499370432610, 3.252606517456513302E-15 ) ) ;
#1108=FACE_OUTER_BOUND ( 'NONE', #2742, .T. ) ;
#1115=DIRECTION ( 'NONE',  ( 1.000000000000000000, 0.000000000000000000, 0.000000000000000000 ) ) ;
#1116=EDGE_CURVE ( 'NONE', #1461, #1923, #2568, .T. ) ;
#1129=VECTOR ( 'NONE', #2895, 1000.000000000000114 ) ;
#1132=DIRECTION ( 'NONE',  ( -0.5000000000000051070, 0.000000000000000000, 0.8660254037844355990 ) ) ;
#1135=DIRECTION ( 'NONE',  ( 0.000000000000000000, -1.287488025362403787E-15, -1.000000000000000000 ) ) ;
#1141=STYLED_ITEM ( 'NONE', ( #908 ), #1999 ) ;
#1142=ORIENTED_EDGE ( 'NONE', *, *, #4505, .F. ) ;
#1146=CARTESIAN_POINT ( 'NONE',  ( 0.000000000000000000, 0.000000000000000000, 0.000000000000000000 ) ) ;
#1172=DIRECTION ( 'NONE',  ( -0.000000000000000000, 0.8660254037844390407, 0.4999999999999993339 ) ) ;
#1179=VERTEX_POINT ( 'NONE', #1664 ) ;
#1186=ORIENTED_EDGE ( 'NONE', *, *, #2562, .T. ) ;
#1191=DIRECTION ( 'NONE',  ( 0.000000000000000000, 0.000000000000000000, -1.000000000000000000 ) ) ;
#1195=DIRECTION ( 'NONE',  ( -1.000000000000000000, -0.000000000000000000, -0.000000000000000000 ) ) ;
#1196=LINE ( 'NONE', #3519, #1378 ) ;
#1197=DIRECTION ( 'NONE',  ( 0.000000000000000000, 0.000000000000000000, -1.000000000000000000 ) ) ;
#1207=DIRECTION ( 'NONE',  ( 1.000000000000000000, 0.000000000000000000, 0.000000000000000000 ) ) ;
#1208=CARTESIAN_POINT ( 'NONE',  ( 2.500000000000000000, 0.000000000000000000, 0.000000000000000000 ) ) ;
#1209=VERTEX_POINT ( 'NONE', #4775 ) ;
#1217=EDGE_CURVE ( 'NONE', #1044, #2709, #4037, .T. ) ;
#1218=ORIENTED_EDGE ( 'NONE', *, *, #1217, .T. ) ;
#1220=AXIS2_PLACEMENT_3D ( 'NONE', #3313, #2212, #4477 ) ;
#1237=ORIENTED_EDGE ( 'NONE', *, *, #4276, .F. ) ;
#1254=EDGE_CURVE ( 'NONE', #340, #4850, #641, .T. ) ;
#1259=DIRECTION ( 'NONE',  ( 0.000000000000000000, 0.000000000000000000, 1.000000000000000000 ) ) ;
#1268=ORIENTED_EDGE ( 'NONE', *, *, #3417, .T. ) ;
#1277=ORIENTED_EDGE ( 'NONE', *, *, #547, .T. ) ;
#1280=CIRCLE ( 'NONE', #3357, 4.000000000000000000 ) ;
#1281=LINE ( 'NONE', #4330, #3316 ) ;
#1287=CIRCLE ( 'NONE', #4074, 2.500000000000001332 ) ;
#1294=DIRECTION ( 'NONE',  ( -1.000000000000000000, -0.000000000000000000, -0.000000000000000000 ) ) ;
#1296=LINE ( 'NONE', #3591, #915 ) ;
#1302=PLANE ( 'NONE',  #3212 ) ;
#1308=CARTESIAN_POINT ( 'NONE',  ( 2.500000000000000000, 0.000000000000000000, 0.000000000000000000 ) ) ;
#1309=CIRCLE ( 'NONE', #3684, 0.2500000000000002220 ) ;
#1320=VERTEX_POINT ( 'NONE', #564 ) ;
#1332=ORIENTED_EDGE ( 'NONE', *, *, #2562, .F. ) ;
#1333=EDGE_CURVE ( 'NONE', #4568, #484, #2018, .T. ) ;
#1334=CARTESIAN_POINT ( 'NONE',  ( 0.000000000000000000, 5.051668046482832750E-16, -4.000000000000000000 ) ) ;
#1342=CARTESIAN_POINT ( 'NONE',  ( 5.200000000000002842, 0.000000000000000000, 0.000000000000000000 ) ) ;
#1346=EDGE_LOOP ( 'NONE', ( #2389, #3226, #794 ) ) ;
#1354=EDGE_LOOP ( 'NONE', ( #4517, #3277, #3266, #262 ) ) ;
#1360=EDGE_CURVE ( 'NONE', #3389, #216, #2941, .T. ) ;
#1367=ORIENTED_EDGE ( 'NONE', *, *, #4600, .F. ) ;
#1371=CARTESIAN_POINT ( 'NONE',  ( 5.000000000000004441, 5.204748896376250699E-16, -4.250000000000000000 ) ) ;
#1372=PLANE ( 'NONE',  #4488 ) ;
#1378=VECTOR ( 'NONE', #3497, 1000.000000000000114 ) ;
#1386=( LENGTH_UNIT ( ) NAMED_UNIT ( * ) SI_UNIT ( .MILLI., .METRE. ) );
#1393=AXIS2_PLACEMENT_3D ( 'NONE', #629, #3391, #4433 ) ;
#1395=VERTEX_POINT ( 'NONE', #1458 ) ;
#1410=ORIENTED_EDGE ( 'NONE', *, *, #4276, .T. ) ;
#1411=ORIENTED_EDGE ( 'NONE', *, *, #547, .F. ) ;
#1417=EDGE_CURVE ( 'NONE', #3810, #1179, #4402, .T. ) ;
#1422=ORIENTED_EDGE ( 'NONE', *, *, #655, .F. ) ;
#1423=DIRECTION ( 'NONE',  ( 0.000000000000000000, -0.4999999999999993894, 0.8660254037844389297 ) ) ;
#1427=CARTESIAN_POINT ( 'NONE',  ( 0.2500000000000002220, 5.204748896376250699E-16, -4.250000000000000000 ) ) ;
#1437=VECTOR ( 'NONE', #3347, 1000.000000000000000 ) ;
#1442=AXIS2_PLACEMENT_3D ( 'NONE', #682, #1830, #1086 ) ;
#1452=AXIS2_PLACEMENT_3D ( 'NONE', #2221, #2601, #3722 ) ;
#1458=CARTESIAN_POINT ( 'NONE',  ( 2.500000000000000000, -1.178949249685218303, -2.041999999999998039 ) ) ;
#1461=VERTEX_POINT ( 'NONE', #1427 ) ;
#1462=AXIS2_PLACEMENT_3D ( 'NONE', #1037, #4460, #4062 ) ;
#1474=LINE ( 'NONE', #2993, #3071 ) ;
#1476=DIRECTION ( 'NONE',  ( 0.000000000000000000, 0.000000000000000000, 1.000000000000000000 ) ) ;
#1477=ORIENTED_EDGE ( 'NONE', *, *, #4419, .F. ) ;
#1492=CARTESIAN_POINT ( 'NONE',  ( 2.500000000000000000, 2.357898499370433054, -1.951563910473907981E-15 ) ) ;
#1495=( GEOMETRIC_REPRESENTATION_CONTEXT ( 3 ) GLOBAL_UNCERTAINTY_ASSIGNED_CONTEXT ( ( #2332 ) ) GLOBAL_UNIT_ASSIGNED_CONTEXT ( ( #1386, #309, #3637 ) ) REPRESENTATION_CONTEXT ( 'NONE', 'WORKASPACE' ) );
#1498=DIRECTION ( 'NONE',  ( 0.000000000000000000, -0.5000000000000012212, -0.8660254037844380415 ) ) ;
#1513=ORIENTED_EDGE ( 'NONE', *, *, #2839, .F. ) ;
#1514=LINE ( 'NONE', #2728, #4549 ) ;
#1520=AXIS2_PLACEMENT_3D ( 'NONE', #3046, #3438, #2673 ) ;
#1526=CIRCLE ( 'NONE', #3770, 2.041999999999999815 ) ;
#1528=DIRECTION ( 'NONE',  ( 0.000000000000000000, 0.000000000000000000, 1.000000000000000000 ) ) ;
#1532=VECTOR ( 'NONE', #1102, 1000.000000000000000 ) ;
#1565=CARTESIAN_POINT ( 'NONE',  ( 2.500000000000000000, 3.004629197474318851E-15, 2.042000000000000259 ) ) ;
#1566=FACE_OUTER_BOUND ( 'NONE', #1632, .T. ) ;
#1568=CARTESIAN_POINT ( 'NONE',  ( 2.500000000000000000, 1.178949249685218525, 2.041999999999999371 ) ) ;
#1569=CARTESIAN_POINT ( 'NONE',  ( 0.000000000000000000, 1.178949249685213863, -2.042000000000001148 ) ) ;
#1588=DIRECTION ( 'NONE',  ( 0.000000000000000000, 0.000000000000000000, 1.000000000000000000 ) ) ;
#1609=AXIS2_PLACEMENT_3D ( 'NONE', #1658, #4616, #1191 ) ;
#1621=VECTOR ( 'NONE', #2537, 1000.000000000000000 ) ;
#1632=EDGE_LOOP ( 'NONE', ( #2406, #416, #3683 ) ) ;
#1640=EDGE_LOOP ( 'NONE', ( #4522, #2809 ) ) ;
#1658=CARTESIAN_POINT ( 'NONE',  ( 5.200000000000002842, 0.000000000000000000, -2.700000000000001066 ) ) ;
#1662=ADVANCED_FACE ( 'NONE', ( #3221 ), #2982, .F. ) ;
#1663=EDGE_LOOP ( 'NONE', ( #3382, #4596, #3244, #1237 ) ) ;
#1664=CARTESIAN_POINT ( 'NONE',  ( 25.00000000000000000, 0.000000000000000000, 2.055000000000000160 ) ) ;
#1666=DIRECTION ( 'NONE',  ( -0.000000000000000000, 0.000000000000000000, 1.000000000000000000 ) ) ;
#1675=CARTESIAN_POINT ( 'NONE',  ( 2.500000000000000000, 1.178949249685213863, -2.042000000000001148 ) ) ;
#1676=SURFACE_SIDE_STYLE ('',( #4379 ) ) ;
#1686=AXIS2_PLACEMENT_3D ( 'NONE', #4693, #2800, #3128 ) ;
#1689=CARTESIAN_POINT ( 'NONE',  ( 5.000000000000000888, 0.000000000000000000, 0.000000000000000000 ) ) ;
#1704=VECTOR ( 'NONE', #455, 1000.000000000000000 ) ;
#1706=EDGE_CURVE ( 'NONE', #4182, #115, #981, .T. ) ;
#1709=DIRECTION ( 'NONE',  ( 0.000000000000000000, 0.000000000000000000, -1.000000000000000000 ) ) ;
#1712=ORIENTED_EDGE ( 'NONE', *, *, #3804, .F. ) ;
#1713=DIRECTION ( 'NONE',  ( 0.000000000000000000, 0.000000000000000000, -1.000000000000000000 ) ) ;
#1716=VERTEX_POINT ( 'NONE', #1334 ) ;
#1727=DIRECTION ( 'NONE',  ( -1.000000000000000000, -0.000000000000000000, -0.000000000000000000 ) ) ;
#1734=DIRECTION ( 'NONE',  ( -0.000000000000000000, 1.000000000000000000, 1.224646799147353207E-16 ) ) ;
#1744=ORIENTED_EDGE ( 'NONE', *, *, #986, .T. ) ;
#1746=ADVANCED_FACE ( 'NONE', ( #154 ), #2118, .T. ) ;
#1747=DIRECTION ( 'NONE',  ( 0.000000000000000000, 0.4999999999999993339, -0.8660254037844390407 ) ) ;
#1761=FACE_OUTER_BOUND ( 'NONE', #2254, .T. ) ;
#1767=CIRCLE ( 'NONE', #2255, 2.041999999999999815 ) ;
#1772=VECTOR ( 'NONE', #1747, 1000.000000000000000 ) ;
#1776=AXIS2_PLACEMENT_3D ( 'NONE', #330, #1902, #1476 ) ;
#1777=AXIS2_PLACEMENT_3D ( 'NONE', #2052, #1294, #4320 ) ;
#1791=AXIS2_PLACEMENT_3D ( 'NONE', #2409, #447, #1528 ) ;
#1795=CIRCLE ( 'NONE', #3008, 2.041999999999999815 ) ;
#1796=CARTESIAN_POINT ( 'NONE',  ( 0.2500000000000002220, 0.000000000000000000, 0.000000000000000000 ) ) ;
#1799=EDGE_LOOP ( 'NONE', ( #4029, #4890, #424, #1186 ) ) ;
#1807=CARTESIAN_POINT ( 'NONE',  ( 2.500000000000000000, -2.629050547790028551E-15, -2.041999999999999815 ) ) ;
#1819=VERTEX_POINT ( 'NONE', #4861 ) ;
#1830=DIRECTION ( 'NONE',  ( -1.000000000000000000, -0.000000000000000000, -0.000000000000000000 ) ) ;
#1839=EDGE_CURVE ( 'NONE', #2615, #2974, #1054, .T. ) ;
#1841=EDGE_LOOP ( 'NONE', ( #4765, #591, #2669, #1744, #616 ) ) ;
#1855=FACE_OUTER_BOUND ( 'NONE', #1841, .T. ) ;
#1859=ORIENTED_EDGE ( 'NONE', *, *, #172, .F. ) ;
#1860=PLANE ( 'NONE',  #1393 ) ;
#1865=AXIS2_PLACEMENT_3D ( 'NONE', #1342, #2802, #3617 ) ;
#1874=AXIS2_PLACEMENT_3D ( 'NONE', #1492, #2227, #3727 ) ;
#1877=EDGE_CURVE ( 'NONE', #1320, #3389, #2992, .T. ) ;
#1892=DIRECTION ( 'NONE',  ( 0.000000000000000000, 0.000000000000000000, 1.000000000000000000 ) ) ;
#1894=ORIENTED_EDGE ( 'NONE', *, *, #1217, .F. ) ;
#1901=FACE_OUTER_BOUND ( 'NONE', #735, .T. ) ;
#1902=DIRECTION ( 'NONE',  ( -1.000000000000000000, -0.000000000000000000, -0.000000000000000000 ) ) ;
#1903=EDGE_CURVE ( 'NONE', #1923, #3747, #2500, .T. ) ;
#1906=CYLINDRICAL_SURFACE ( 'NONE', #1791, 4.250000000000000000 ) ;
#1918=AXIS2_PLACEMENT_3D ( 'NONE', #1146, #2700, #1115 ) ;
#1923=VERTEX_POINT ( 'NONE', #4177 ) ;
#1926=CIRCLE ( 'NONE', #4732, 4.250000000000000000 ) ;
#1961=LINE ( 'NONE', #466, #3689 ) ;
#1974=CARTESIAN_POINT ( 'NONE',  ( 2.500000000000000000, -1.768423874527823791, -1.020999999999998353 ) ) ;
#1978=PRODUCT_DEFINITION_CONTEXT ( 'detailed design', #609, 'design' ) ;
#1980=FACE_OUTER_BOUND ( 'NONE', #2776, .T. ) ;
#1989=VERTEX_POINT ( 'NONE', #2482 ) ;
#1991=CARTESIAN_POINT ( 'NONE',  ( 2.500000000000000000, 0.000000000000000000, 0.000000000000000000 ) ) ;
#1999=MANIFOLD_SOLID_BREP ( 'Hex', #2272 ) ;
#2007=ORIENTED_EDGE ( 'NONE', *, *, #3042, .F. ) ;
#2018=CIRCLE ( 'NONE', #644, 2.700000000000001066 ) ;
#2023=DIRECTION ( 'NONE',  ( 1.000000000000000000, 0.000000000000000000, 0.000000000000000000 ) ) ;
#2026=CARTESIAN_POINT ( 'NONE',  ( 25.00000000000000000, 2.789133085058098087E-16, -2.055000000000000160 ) ) ;
#2028=VECTOR ( 'NONE', #1132, 1000.000000000000114 ) ;
#2037=FACE_OUTER_BOUND ( 'NONE', #331, .T. ) ;
#2041=ORIENTED_EDGE ( 'NONE', *, *, #4698, .F. ) ;
#2048=ORIENTED_EDGE ( 'NONE', *, *, #3417, .F. ) ;
#2049=ORIENTED_EDGE ( 'NONE', *, *, #4411, .F. ) ;
#2052=CARTESIAN_POINT ( 'NONE',  ( -31.74999999999995737, 0.000000000000000000, 0.000000000000000000 ) ) ;
#2061=SURFACE_STYLE_USAGE ( .BOTH. , #1676 ) ;
#2069=ORIENTED_EDGE ( 'NONE', *, *, #664, .T. ) ;
#2077=ADVANCED_FACE ( 'NONE', ( #4954 ), #1372, .T. ) ;
#2084=FACE_OUTER_BOUND ( 'NONE', #1663, .T. ) ;
#2087=ORIENTED_EDGE ( 'NONE', *, *, #869, .T. ) ;
#2107=CIRCLE ( 'NONE', #2580, 2.041999999999999815 ) ;
#2118=CYLINDRICAL_SURFACE ( 'NONE', #3145, 2.500000000000000888 ) ;
#2133=ORIENTED_EDGE ( 'NONE', *, *, #2624, .T. ) ;
#2136=CARTESIAN_POINT ( 'NONE',  ( 5.000000000000000888, 4.250000000000000000, 0.000000000000000000 ) ) ;
#2137=EDGE_CURVE ( 'NONE', #1989, #45, #1196, .T. ) ;
#2139=DIRECTION ( 'NONE',  ( 0.000000000000000000, 0.000000000000000000, 1.000000000000000000 ) ) ;
#2153=APPLICATION_CONTEXT ( 'automotive_design' ) ;
#2157=CARTESIAN_POINT ( 'NONE',  ( 0.2500000000000002220, 0.000000000000000000, 0.000000000000000000 ) ) ;
#2159=CIRCLE ( 'NONE', #3749, 2.055000000000000160 ) ;
#2166=ADVANCED_FACE ( 'NONE', ( #40 ), #4720, .T. ) ;
#2173=ORIENTED_EDGE ( 'NONE', *, *, #1877, .T. ) ;
#2179=ORIENTED_EDGE ( 'NONE', *, *, #4409, .F. ) ;
#2182=CARTESIAN_POINT ( 'NONE',  ( 0.000000000000000000, -1.178949249685213863, 2.042000000000002924 ) ) ;
#2183=DIRECTION ( 'NONE',  ( 0.000000000000000000, 0.000000000000000000, -1.000000000000000000 ) ) ;
#2212=DIRECTION ( 'NONE',  ( 1.000000000000000000, 0.000000000000000000, 0.000000000000000000 ) ) ;
#2221=CARTESIAN_POINT ( 'NONE',  ( 5.000000000000000888, 0.000000000000000000, 0.000000000000000000 ) ) ;
#2227=DIRECTION ( 'NONE',  ( 0.000000000000000000, 0.8660254037844380415, -0.5000000000000012212 ) ) ;
#2238=CARTESIAN_POINT ( 'NONE',  ( 2.500000000000000000, 2.357898499370433054, -1.951563910473907981E-15 ) ) ;
#2250=FACE_OUTER_BOUND ( 'NONE', #3428, .T. ) ;
#2254=EDGE_LOOP ( 'NONE', ( #2849, #274, #1410, #2600 ) ) ;
#2255=AXIS2_PLACEMENT_3D ( 'NONE', #700, #3387, #2963 ) ;
#2256=VECTOR ( 'NONE', #304, 1000.000000000000000 ) ;
#2272=CLOSED_SHELL ( 'NONE', ( #999, #783, #1662, #71, #1746, #3505, #3879, #2459, #3204, #4444, #3625, #2166, #3583, #220, #3529, #2962, #120, #2077, #70, #387, #2957, #355, #3652, #494, #47, #998, #2851 ) ) ;
#2278=EDGE_CURVE ( 'NONE', #1461, #1716, #1309, .T. ) ;
#2297=DIRECTION ( 'NONE',  ( -1.000000000000000000, -0.000000000000000000, -0.000000000000000000 ) ) ;
#2304=LINE ( 'NONE', #3826, #2028 ) ;
#2307=PRODUCT_DEFINITION ( 'UNKNOWN', '', #3822, #1978 ) ;
#2308=ORIENTED_EDGE ( 'NONE', *, *, #4024, .T. ) ;
#2323=DIRECTION ( 'NONE',  ( 0.000000000000000000, -0.5000000000000011102, -0.8660254037844379305 ) ) ;
#2332=UNCERTAINTY_MEASURE_WITH_UNIT (LENGTH_MEASURE( 1.000000000000000082E-05 ), #1386, 'distance_accuracy_value', 'NONE');
#2335=CARTESIAN_POINT ( 'NONE',  ( 2.500000000000000000, -1.178949249685213863, 2.042000000000002924 ) ) ;
#2336=FACE_OUTER_BOUND ( 'NONE', #2713, .T. ) ;
#2339=AXIS2_PLACEMENT_3D ( 'NONE', #3825, #2365, #3140 ) ;
#2351=EDGE_CURVE ( 'NONE', #2431, #3852, #4869, .T. ) ;
#2365=DIRECTION ( 'NONE',  ( 1.000000000000000000, 0.000000000000000000, 0.000000000000000000 ) ) ;
#2379=EDGE_CURVE ( 'NONE', #3315, #484, #4100, .T. ) ;
#2389=ORIENTED_EDGE ( 'NONE', *, *, #2351, .T. ) ;
#2393=CARTESIAN_POINT ( 'NONE',  ( 0.2500000000000002220, 0.000000000000000000, 0.000000000000000000 ) ) ;
#2406=ORIENTED_EDGE ( 'NONE', *, *, #3705, .F. ) ;
#2409=CARTESIAN_POINT ( 'NONE',  ( -31.74999999999995737, 0.000000000000000000, 0.000000000000000000 ) ) ;
#2418=AXIS2_PLACEMENT_3D ( 'NONE', #3271, #4719, #608 ) ;
#2428=PLANE ( 'NONE',  #1686 ) ;
#2431=VERTEX_POINT ( 'NONE', #2971 ) ;
#2436=ORIENTED_EDGE ( 'NONE', *, *, #1839, .F. ) ;
#2439=PLANE ( 'NONE',  #2681 ) ;
#2440=FILL_AREA_STYLE_COLOUR ( '', #3300 ) ;
#2441=CARTESIAN_POINT ( 'NONE',  ( 2.500000000000000000, 2.357898499370433054, -1.951563910473907981E-15 ) ) ;
#2450=ORIENTED_EDGE ( 'NONE', *, *, #3269, .T. ) ;
#2454=DIRECTION ( 'NONE',  ( -1.000000000000000000, -0.000000000000000000, -0.000000000000000000 ) ) ;
#2459=ADVANCED_FACE ( 'NONE', ( #365 ), #290, .T. ) ;
#2467=ORIENTED_EDGE ( 'NONE', *, *, #3705, .T. ) ;
#2482=CARTESIAN_POINT ( 'NONE',  ( 2.500000000000000000, -1.768423874527823569, 1.021000000000002794 ) ) ;
#2500=CIRCLE ( 'NONE', #339, 0.2500000000000002220 ) ;
#2503=CARTESIAN_POINT ( 'NONE',  ( 24.55500000000002103, 0.000000000000000000, 0.000000000000000000 ) ) ;
#2505=AXIS2_PLACEMENT_3D ( 'NONE', #4684, #2792, #4764 ) ;
#2511=DIRECTION ( 'NONE',  ( 0.000000000000000000, 0.000000000000000000, 1.000000000000000000 ) ) ;
#2516=CARTESIAN_POINT ( 'NONE',  ( 0.000000000000000000, 1.178949249685218525, 2.041999999999999371 ) ) ;
#2534=EDGE_LOOP ( 'NONE', ( #3489, #434, #2007 ) ) ;
#2535=CARTESIAN_POINT ( 'NONE',  ( 2.500000000000000000, -1.178949249685213863, 2.042000000000002924 ) ) ;
#2537=DIRECTION ( 'NONE',  ( -0.7071067811865306973, 0.000000000000000000, 0.7071067811865643371 ) ) ;
#2538=ORIENTED_EDGE ( 'NONE', *, *, #1839, .T. ) ;
#2559=AXIS2_PLACEMENT_3D ( 'NONE', #2503, #3554, #480 ) ;
#2562=EDGE_CURVE ( 'NONE', #1923, #1461, #1926, .T. ) ;
#2565=DIRECTION ( 'NONE',  ( 0.000000000000000000, -0.4999999999999993894, 0.8660254037844389297 ) ) ;
#2568=CIRCLE ( 'NONE', #3678, 4.250000000000000000 ) ;
#2580=AXIS2_PLACEMENT_3D ( 'NONE', #3050, #3791, #1892 ) ;
#2594=FACE_OUTER_BOUND ( 'NONE', #3, .T. ) ;
#2600=ORIENTED_EDGE ( 'NONE', *, *, #869, .F. ) ;
#2601=DIRECTION ( 'NONE',  ( -1.000000000000000000, -0.000000000000000000, -0.000000000000000000 ) ) ;
#2611=CARTESIAN_POINT ( 'NONE',  ( 2.500000000000000000, 2.357898499370433054, -1.951563910473907981E-15 ) ) ;
#2612=CARTESIAN_POINT ( 'NONE',  ( 2.500000000000000000, 2.357898499370433054, -1.951563910473907981E-15 ) ) ;
#2615=VERTEX_POINT ( 'NONE', #521 ) ;
#2618=CARTESIAN_POINT ( 'NONE',  ( 2.500000000000000000, 2.357898499370433054, -1.951563910473907981E-15 ) ) ;
#2624=EDGE_CURVE ( 'NONE', #1209, #4568, #970, .T. ) ;
#2652=CONICAL_SURFACE ( 'NONE', #804, 2.041999999999999815, 1.047197551196591858 ) ;
#2655=VECTOR ( 'NONE', #285, 1000.000000000000000 ) ;
#2665=LINE ( 'NONE', #774, #183 ) ;
#2669=ORIENTED_EDGE ( 'NONE', *, *, #3042, .T. ) ;
#2673=DIRECTION ( 'NONE',  ( 0.000000000000000000, 0.000000000000000000, -1.000000000000000000 ) ) ;
#2681=AXIS2_PLACEMENT_3D ( 'NONE', #778, #2813, #408 ) ;
#2688=CARTESIAN_POINT ( 'NONE',  ( 0.000000000000000000, 0.000000000000000000, 0.000000000000000000 ) ) ;
#2699=ORIENTED_EDGE ( 'NONE', *, *, #655, .T. ) ;
#2700=DIRECTION ( 'NONE',  ( 0.000000000000000000, 0.000000000000000000, 1.000000000000000000 ) ) ;
#2709=VERTEX_POINT ( 'NONE', #2516 ) ;
#2711=PLANE ( 'NONE',  #895 ) ;
#2713=EDGE_LOOP ( 'NONE', ( #360, #2087, #1277, #3673 ) ) ;
#2723=CARTESIAN_POINT ( 'NONE',  ( 0.2500000000000002220, 0.000000000000000000, 0.000000000000000000 ) ) ;
#2725=CARTESIAN_POINT ( 'NONE',  ( 2.500000000000000000, -1.178949249685213863, 2.042000000000002924 ) ) ;
#2728=CARTESIAN_POINT ( 'NONE',  ( 2.500000000000000000, -2.357898499370432610, 3.252606517456513302E-15 ) ) ;
#2729=LINE ( 'NONE', #4247, #4803 ) ;
#2732=ORIENTED_EDGE ( 'NONE', *, *, #986, .F. ) ;
#2738=DIRECTION ( 'NONE',  ( -1.000000000000000000, -0.000000000000000000, -0.000000000000000000 ) ) ;
#2742=EDGE_LOOP ( 'NONE', ( #769, #1367, #98, #4777, #16 ) ) ;
#2769=DIRECTION ( 'NONE',  ( -1.000000000000000000, -0.000000000000000000, -0.000000000000000000 ) ) ;
#2776=EDGE_LOOP ( 'NONE', ( #1894, #2048, #2173, #3511, #4833 ) ) ;
#2792=DIRECTION ( 'NONE',  ( -1.000000000000000000, -0.000000000000000000, -0.000000000000000000 ) ) ;
#2800=DIRECTION ( 'NONE',  ( 1.000000000000000000, 0.000000000000000000, 0.000000000000000000 ) ) ;
#2802=DIRECTION ( 'NONE',  ( 1.000000000000000000, 0.000000000000000000, 0.000000000000000000 ) ) ;
#2809=ORIENTED_EDGE ( 'NONE', *, *, #3468, .T. ) ;
#2810=EDGE_CURVE ( 'NONE', #45, #4182, #329, .T. ) ;
#2813=DIRECTION ( 'NONE',  ( 0.000000000000000000, 0.8660254037844380415, -0.5000000000000011102 ) ) ;
#2835=AXIS2_PLACEMENT_3D ( 'NONE', #2441, #128, #3189 ) ;
#2839=EDGE_CURVE ( 'NONE', #645, #1395, #3408, .T. ) ;
#2841=CIRCLE ( 'NONE', #1865, 2.500000000000000888 ) ;
#2849=ORIENTED_EDGE ( 'NONE', *, *, #3475, .F. ) ;
#2850=AXIS2_PLACEMENT_3D ( 'NONE', #1022, #949, #2183 ) ;
#2851=ADVANCED_FACE ( 'NONE', ( #1855 ), #3293, .F. ) ;
#2853=CARTESIAN_POINT ( 'NONE',  ( 0.000000000000000000, -2.357898499370432610, 3.252606517456513302E-15 ) ) ;
#2880=EDGE_LOOP ( 'NONE', ( #4392, #1513, #3048 ) ) ;
#2883=ORIENTED_EDGE ( 'NONE', *, *, #2905, .T. ) ;
#2884=VECTOR ( 'NONE', #4194, 1000.000000000000000 ) ;
#2887=ORIENTED_EDGE ( 'NONE', *, *, #4724, .F. ) ;
#2895=DIRECTION ( 'NONE',  ( 0.000000000000000000, -0.4999999999999993894, 0.8660254037844389297 ) ) ;
#2899=CIRCLE ( 'NONE', #1220, 2.500000000000000888 ) ;
#2905=EDGE_CURVE ( 'NONE', #4296, #645, #1767, .T. ) ;
#2914=EDGE_LOOP ( 'NONE', ( #2308, #138, #1065, #397 ) ) ;
#2929=VERTEX_POINT ( 'NONE', #4179 ) ;
#2930=EDGE_CURVE ( 'NONE', #3315, #1209, #2899, .T. ) ;
#2937=DIRECTION ( 'NONE',  ( -1.000000000000000000, -0.000000000000000000, -0.000000000000000000 ) ) ;
#2941=LINE ( 'NONE', #2618, #1049 ) ;
#2957=ADVANCED_FACE ( 'NONE', ( #4585 ), #3086, .F. ) ;
#2958=ORIENTED_EDGE ( 'NONE', *, *, #1254, .F. ) ;
#2962=ADVANCED_FACE ( 'NONE', ( #1901 ), #2711, .F. ) ;
#2963=DIRECTION ( 'NONE',  ( 0.000000000000000000, 0.000000000000000000, 1.000000000000000000 ) ) ;
#2967=VECTOR ( 'NONE', #481, 999.9999999999998863 ) ;
#2969=FILL_AREA_STYLE ('',( #4456 ) ) ;
#2971=CARTESIAN_POINT ( 'NONE',  ( 2.500000000000000000, 1.768423874527822681, -1.021000000000002794 ) ) ;
#2974=VERTEX_POINT ( 'NONE', #773 ) ;
#2980=EDGE_LOOP ( 'NONE', ( #211, #4486, #706, #789 ) ) ;
#2982=TOROIDAL_SURFACE ( 'NONE', #3610, 2.700000000000001066, 0.2000000000000000111 ) ;
#2987=VECTOR ( 'NONE', #3039, 1000.000000000000000 ) ;
#2992=LINE ( 'NONE', #2611, #3691 ) ;
#2993=CARTESIAN_POINT ( 'NONE',  ( 25.00000000000000000, 2.516649172247811061E-16, -2.055000000000000160 ) ) ;
#2998=EDGE_CURVE ( 'NONE', #571, #115, #1961, .T. ) ;
#3008=AXIS2_PLACEMENT_3D ( 'NONE', #1308, #4733, #1259 ) ;
#3013=CARTESIAN_POINT ( 'NONE',  ( 0.000000000000000000, 0.000000000000000000, 4.000000000000000000 ) ) ;
#3020=ORIENTED_EDGE ( 'NONE', *, *, #2810, .T. ) ;
#3028=EDGE_LOOP ( 'NONE', ( #2049, #764, #2883, #4416, #4493 ) ) ;
#3039=DIRECTION ( 'NONE',  ( -1.000000000000000000, -0.000000000000000000, -0.000000000000000000 ) ) ;
#3042=EDGE_CURVE ( 'NONE', #1050, #3389, #1526, .T. ) ;
#3046=CARTESIAN_POINT ( 'NONE',  ( 25.00000000000000000, 2.055000000000000160, 0.000000000000000000 ) ) ;
#3048=ORIENTED_EDGE ( 'NONE', *, *, #2905, .F. ) ;
#3050=CARTESIAN_POINT ( 'NONE',  ( 2.500000000000000000, 0.000000000000000000, 0.000000000000000000 ) ) ;
#3058=EDGE_CURVE ( 'NONE', #340, #1461, #857, .T. ) ;
#3068=CARTESIAN_POINT ( 'NONE',  ( 2.500000000000000000, 1.768423874527824902, 1.020999999999999019 ) ) ;
#3071=VECTOR ( 'NONE', #3859, 1000.000000000000000 ) ;
#3075=TOROIDAL_SURFACE ( 'NONE', #4341, 2.700000000000001066, 0.2000000000000000111 ) ;
#3084=DIRECTION ( 'NONE',  ( 0.000000000000000000, -0.4999999999999992784, 0.8660254037844389297 ) ) ;
#3086=PLANE ( 'NONE',  #2339 ) ;
#3087=TOROIDAL_SURFACE ( 'NONE', #3631, 4.000000000000000000, 0.2500000000000000000 ) ;
#3093=DIRECTION ( 'NONE',  ( 0.000000000000000000, 0.000000000000000000, 1.000000000000000000 ) ) ;
#3094=CARTESIAN_POINT ( 'NONE',  ( -31.74999999999995737, 5.204748896376250699E-16, -4.250000000000000000 ) ) ;
#3106=CARTESIAN_POINT ( 'NONE',  ( 2.500000000000000000, 1.178949249685213863, -2.042000000000001148 ) ) ;
#3115=CARTESIAN_POINT ( 'NONE',  ( 5.200000000000002842, 0.000000000000000000, 0.000000000000000000 ) ) ;
#3116=DIRECTION ( 'NONE',  ( -0.000000000000000000, 1.471414886128461471E-15, 1.000000000000000000 ) ) ;
#3119=EDGE_CURVE ( 'NONE', #1989, #1050, #182, .T. ) ;
#3122=DIRECTION ( 'NONE',  ( 0.000000000000000000, 0.000000000000000000, 1.000000000000000000 ) ) ;
#3128=DIRECTION ( 'NONE',  ( 0.000000000000000000, 0.000000000000000000, -1.000000000000000000 ) ) ;
#3130=LINE ( 'NONE', #3106, #1704 ) ;
#3133=LINE ( 'NONE', #3900, #2967 ) ;
#3140=DIRECTION ( 'NONE',  ( 0.000000000000000000, 0.000000000000000000, -1.000000000000000000 ) ) ;
#3145=AXIS2_PLACEMENT_3D ( 'NONE', #207, #1727, #2139 ) ;
#3149=CONICAL_SURFACE ( 'NONE', #3379, 2.055000000000000160, 0.7853981633974721488 ) ;
#3155=VECTOR ( 'NONE', #2738, 1000.000000000000000 ) ;
#3161=ORIENTED_EDGE ( 'NONE', *, *, #4704, .T. ) ;
#3164=DIRECTION ( 'NONE',  ( 0.000000000000000000, 0.000000000000000000, -1.000000000000000000 ) ) ;
#3189=DIRECTION ( 'NONE',  ( 0.000000000000000000, 0.4999999999999993894, -0.8660254037844389297 ) ) ;
#3203=VECTOR ( 'NONE', #4699, 1000.000000000000114 ) ;
#3204=ADVANCED_FACE ( 'NONE', ( #1761 ), #3149, .T. ) ;
#3212=AXIS2_PLACEMENT_3D ( 'NONE', #4300, #3881, #3164 ) ;
#3215=DIRECTION ( 'NONE',  ( 0.000000000000000000, 0.000000000000000000, -1.000000000000000000 ) ) ;
#3221=FACE_OUTER_BOUND ( 'NONE', #1354, .T. ) ;
#3226=ORIENTED_EDGE ( 'NONE', *, *, #146, .T. ) ;
#3233=AXIS2_PLACEMENT_3D ( 'NONE', #4135, #3414, #1064 ) ;
#3234=DIRECTION ( 'NONE',  ( 0.000000000000000000, 0.000000000000000000, 1.000000000000000000 ) ) ;
#3240=DIRECTION ( 'NONE',  ( 1.000000000000000000, 0.000000000000000000, 0.000000000000000000 ) ) ;
#3242=AXIS2_PLACEMENT_3D ( 'NONE', #1675, #1135, #3435 ) ;
#3244=ORIENTED_EDGE ( 'NONE', *, *, #4825, .F. ) ;
#3250=ORIENTED_EDGE ( 'NONE', *, *, #1877, .F. ) ;
#3254=DIRECTION ( 'NONE',  ( 0.000000000000000000, 0.000000000000000000, 1.000000000000000000 ) ) ;
#3266=ORIENTED_EDGE ( 'NONE', *, *, #1333, .F. ) ;
#3269=EDGE_CURVE ( 'NONE', #484, #4568, #341, .T. ) ;
#3271=CARTESIAN_POINT ( 'NONE',  ( 5.000000000000004441, 0.000000000000000000, 0.000000000000000000 ) ) ;
#3277=ORIENTED_EDGE ( 'NONE', *, *, #2379, .T. ) ;
#3293=CONICAL_SURFACE ( 'NONE', #3933, 2.041999999999999815, 1.047197551196591858 ) ;
#3300=COLOUR_RGB ( '', 0.66274510, 0.83137255, 0.94901961) ;
#3305=EDGE_CURVE ( 'NONE', #2431, #4296, #2107, .T. ) ;
#3310=DIRECTION ( 'NONE',  ( -1.000000000000000000, -0.000000000000000000, -0.000000000000000000 ) ) ;
#3312=CARTESIAN_POINT ( 'NONE',  ( 0.2500000000000002220, 0.000000000000000000, 4.000000000000000000 ) ) ;
#3313=CARTESIAN_POINT ( 'NONE',  ( 5.200000000000002842, 0.000000000000000000, 0.000000000000000000 ) ) ;
#3315=VERTEX_POINT ( 'NONE', #4464 ) ;
#3316=VECTOR ( 'NONE', #3831, 1000.000000000000000 ) ;
#3327=DIRECTION ( 'NONE',  ( -1.000000000000000000, -0.000000000000000000, -0.000000000000000000 ) ) ;
#3336=DIRECTION ( 'NONE',  ( 0.000000000000000000, 0.000000000000000000, 1.000000000000000000 ) ) ;
#3347=DIRECTION ( 'NONE',  ( 0.000000000000000000, 1.000000000000000000, -1.471414886128461471E-15 ) ) ;
#3357=AXIS2_PLACEMENT_3D ( 'NONE', #824, #2297, #3818 ) ;
#3365=DIRECTION ( 'NONE',  ( 0.000000000000000000, -0.5000000000000012212, -0.8660254037844380415 ) ) ;
#3371=CARTESIAN_POINT ( 'NONE',  ( 2.500000000000000000, -1.178949249685213863, 2.042000000000002924 ) ) ;
#3379=AXIS2_PLACEMENT_3D ( 'NONE', #3620, #592, #3254 ) ;
#3381=LINE ( 'NONE', #2725, #4828 ) ;
#3382=ORIENTED_EDGE ( 'NONE', *, *, #4724, .T. ) ;
#3387=DIRECTION ( 'NONE',  ( -1.000000000000000000, -0.000000000000000000, -0.000000000000000000 ) ) ;
#3389=VERTEX_POINT ( 'NONE', #3068 ) ;
#3391=DIRECTION ( 'NONE',  ( 1.000000000000000000, 0.000000000000000000, 0.000000000000000000 ) ) ;
#3405=ORIENTED_EDGE ( 'NONE', *, *, #2998, .F. ) ;
#3407=LINE ( 'NONE', #2612, #1532 ) ;
#3408=LINE ( 'NONE', #1103, #2655 ) ;
#3414=DIRECTION ( 'NONE',  ( 0.000000000000000000, 1.000000000000000000, -1.224646799147353207E-16 ) ) ;
#3417=EDGE_CURVE ( 'NONE', #1320, #1044, #3407, .T. ) ;
#3427=ORIENTED_EDGE ( 'NONE', *, *, #2278, .F. ) ;
#3428=EDGE_LOOP ( 'NONE', ( #2069, #1477, #621, #2179, #1268 ) ) ;
#3434=EDGE_LOOP ( 'NONE', ( #4162, #3442, #1859 ) ) ;
#3435=DIRECTION ( 'NONE',  ( 0.000000000000000000, 1.000000000000000000, -1.287488025362403787E-15 ) ) ;
#3438=DIRECTION ( 'NONE',  ( 1.000000000000000000, 0.000000000000000000, 0.000000000000000000 ) ) ;
#3442=ORIENTED_EDGE ( 'NONE', *, *, #2137, .F. ) ;
#3458=CARTESIAN_POINT ( 'NONE',  ( 2.500000000000000000, 1.178949249685213863, -2.042000000000001148 ) ) ;
#3468=EDGE_CURVE ( 'NONE', #1716, #3747, #348, .T. ) ;
#3469=ORIENTED_EDGE ( 'NONE', *, *, #2137, .T. ) ;
#3475=EDGE_CURVE ( 'NONE', #3810, #4351, #1474, .T. ) ;
#3480=LINE ( 'NONE', #1568, #317 ) ;
#3489=ORIENTED_EDGE ( 'NONE', *, *, #939, .T. ) ;
#3497=DIRECTION ( 'NONE',  ( 0.000000000000000000, -0.5000000000000011102, -0.8660254037844379305 ) ) ;
#3500=DIRECTION ( 'NONE',  ( 0.000000000000000000, 0.4999999999999993339, -0.8660254037844390407 ) ) ;
#3501=DIRECTION ( 'NONE',  ( 0.000000000000000000, 1.000000000000000000, -1.471414886128461471E-15 ) ) ;
#3505=ADVANCED_FACE ( 'NONE', ( #2084 ), #657, .T. ) ;
#3511=ORIENTED_EDGE ( 'NONE', *, *, #1360, .T. ) ;
#3517=( LENGTH_UNIT ( ) NAMED_UNIT ( * ) SI_UNIT ( .MILLI., .METRE. ) );
#3519=CARTESIAN_POINT ( 'NONE',  ( 2.500000000000000000, -1.178949249685213863, 2.042000000000002924 ) ) ;
#3529=ADVANCED_FACE ( 'NONE', ( #1980 ), #909, .T. ) ;
#3551=CARTESIAN_POINT ( 'NONE',  ( 2.500000000000000000, 1.178949249685213863, -2.042000000000001148 ) ) ;
#3552=AXIS2_PLACEMENT_3D ( 'NONE', #868, #142, #1666 ) ;
#3554=DIRECTION ( 'NONE',  ( -1.000000000000000000, -0.000000000000000000, -0.000000000000000000 ) ) ;
#3558=( LENGTH_UNIT ( ) NAMED_UNIT ( * ) SI_UNIT ( .MILLI., .METRE. ) );
#3561=ORIENTED_EDGE ( 'NONE', *, *, #3468, .F. ) ;
#3571=PLANE ( 'NONE',  #3552 ) ;
#3573=EDGE_CURVE ( 'NONE', #4351, #1209, #4333, .T. ) ;
#3580=DIRECTION ( 'NONE',  ( 0.000000000000000000, 0.000000000000000000, 1.000000000000000000 ) ) ;
#3583=ADVANCED_FACE ( 'NONE', ( #50 ), #3075, .F. ) ;
#3591=CARTESIAN_POINT ( 'NONE',  ( -31.74999999999995737, 0.000000000000000000, 4.250000000000000000 ) ) ;
#3598=TOROIDAL_SURFACE ( 'NONE', #4554, 4.000000000000000000, 0.2500000000000000000 ) ;
#3606=DIRECTION ( 'NONE',  ( 1.000000000000000000, 0.000000000000000000, 0.000000000000000000 ) ) ;
#3610=AXIS2_PLACEMENT_3D ( 'NONE', #3942, #3606, #1709 ) ;
#3617=DIRECTION ( 'NONE',  ( 0.000000000000000000, 0.000000000000000000, -1.000000000000000000 ) ) ;
#3620=CARTESIAN_POINT ( 'NONE',  ( 25.00000000000000000, 0.000000000000000000, 0.000000000000000000 ) ) ;
#3625=ADVANCED_FACE ( 'NONE', ( #3672, #3884 ), #4807, .T. ) ;
#3631=AXIS2_PLACEMENT_3D ( 'NONE', #2157, #3310, #2511 ) ;
#3637=( NAMED_UNIT ( * ) SI_UNIT ( $, .STERADIAN. ) SOLID_ANGLE_UNIT ( ) );
#3652=ADVANCED_FACE ( 'NONE', ( #1566 ), #321, .F. ) ;
#3653=EDGE_CURVE ( 'NONE', #4296, #1395, #3130, .T. ) ;
#3654=EDGE_CURVE ( 'NONE', #2615, #1050, #3381, .T. ) ;
#3669=CIRCLE ( 'NONE', #2559, 2.500000000000001332 ) ;
#3672=FACE_BOUND ( 'NONE', #356, .T. ) ;
#3673=ORIENTED_EDGE ( 'NONE', *, *, #2930, .T. ) ;
#3678=AXIS2_PLACEMENT_3D ( 'NONE', #2723, #2023, #475 ) ;
#3683=ORIENTED_EDGE ( 'NONE', *, *, #3119, .F. ) ;
#3684=AXIS2_PLACEMENT_3D ( 'NONE', #214, #1734, #4795 ) ;
#3689=VECTOR ( 'NONE', #27, 1000.000000000000000 ) ;
#3691=VECTOR ( 'NONE', #1423, 1000.000000000000114 ) ;
#3705=EDGE_CURVE ( 'NONE', #2615, #1989, #477, .T. ) ;
#3712=SURFACE_SIDE_STYLE ('',( #681 ) ) ;
#3722=DIRECTION ( 'NONE',  ( 0.000000000000000000, 0.000000000000000000, -1.000000000000000000 ) ) ;
#3727=DIRECTION ( 'NONE',  ( 0.000000000000000000, 0.5000000000000012212, 0.8660254037844380415 ) ) ;
#3740=CARTESIAN_POINT ( 'NONE',  ( 2.500000000000000000, 0.000000000000000000, 0.000000000000000000 ) ) ;
#3747=VERTEX_POINT ( 'NONE', #3013 ) ;
#3749=AXIS2_PLACEMENT_3D ( 'NONE', #3924, #2454, #3234 ) ;
#3750=DIRECTION ( 'NONE',  ( 0.000000000000000000, 0.000000000000000000, -1.000000000000000000 ) ) ;
#3770=AXIS2_PLACEMENT_3D ( 'NONE', #1208, #2769, #798 ) ;
#3779=AXIS2_PLACEMENT_3D ( 'NONE', #2688, #772, #3093 ) ;
#3791=DIRECTION ( 'NONE',  ( -1.000000000000000000, -0.000000000000000000, -0.000000000000000000 ) ) ;
#3794=CARTESIAN_POINT ( 'NONE',  ( 2.500000000000000000, -2.357898499370432610, 3.252606517456513302E-15 ) ) ;
#3804=EDGE_CURVE ( 'NONE', #1209, #3315, #2841, .T. ) ;
#3805=CARTESIAN_POINT ( 'NONE',  ( 2.500000000000000000, 1.178949249685218525, 2.041999999999999371 ) ) ;
#3810=VERTEX_POINT ( 'NONE', #2026 ) ;
#3816=( GEOMETRIC_REPRESENTATION_CONTEXT ( 3 ) GLOBAL_UNCERTAINTY_ASSIGNED_CONTEXT ( ( #830 ) ) GLOBAL_UNIT_ASSIGNED_CONTEXT ( ( #3517, #4867, #4085 ) ) REPRESENTATION_CONTEXT ( 'NONE', 'WORKASPACE' ) );
#3818=DIRECTION ( 'NONE',  ( 0.000000000000000000, 0.000000000000000000, 1.000000000000000000 ) ) ;
#3822=PRODUCT_DEFINITION_FORMATION_WITH_SPECIFIED_SOURCE ( 'ANY', '', #51, .NOT_KNOWN. ) ;
#3825=CARTESIAN_POINT ( 'NONE',  ( 2.500000000000000000, 2.357898499370433054, -1.951563910473907981E-15 ) ) ;
#3826=CARTESIAN_POINT ( 'NONE',  ( 2.500000000000000000, 0.000000000000000000, 2.041999999999999815 ) ) ;
#3827=EDGE_CURVE ( 'NONE', #4850, #1923, #1296, .T. ) ;
#3831=DIRECTION ( 'NONE',  ( 0.000000000000000000, -1.000000000000000000, 1.287488025362403787E-15 ) ) ;
#3852=VERTEX_POINT ( 'NONE', #3551 ) ;
#3859=DIRECTION ( 'NONE',  ( -0.7071067811865306973, 8.659560562355138702E-17, -0.7071067811865643371 ) ) ;
#3861=CYLINDRICAL_SURFACE ( 'NONE', #1776, 2.500000000000000888 ) ;
#3870=EDGE_LOOP ( 'NONE', ( #1072, #1712, #2133, #4289 ) ) ;
#3873=CARTESIAN_POINT ( 'NONE',  ( 0.000000000000000000, 2.357898499370433054, -1.951563910473907981E-15 ) ) ;
#3879=ADVANCED_FACE ( 'NONE', ( #3951, #529 ), #3571, .T. ) ;
#3881=DIRECTION ( 'NONE',  ( 1.000000000000000000, 0.000000000000000000, 0.000000000000000000 ) ) ;
#3884=FACE_OUTER_BOUND ( 'NONE', #4809, .T. ) ;
#3896=DIRECTION ( 'NONE',  ( 0.000000000000000000, 1.000000000000000000, -1.471414886128461471E-15 ) ) ;
#3900=CARTESIAN_POINT ( 'NONE',  ( 0.000000000000000000, 2.357898499370433054, -1.951563910473907981E-15 ) ) ;
#3919=DIRECTION ( 'NONE',  ( 0.000000000000000000, 0.000000000000000000, 1.000000000000000000 ) ) ;
#3924=CARTESIAN_POINT ( 'NONE',  ( 25.00000000000000000, 0.000000000000000000, 0.000000000000000000 ) ) ;
#3926=CARTESIAN_POINT ( 'NONE',  ( -31.74999999999995737, 0.000000000000000000, 2.500000000000000888 ) ) ;
#3933=AXIS2_PLACEMENT_3D ( 'NONE', #4888, #4941, #3336 ) ;
#3942=CARTESIAN_POINT ( 'NONE',  ( 5.200000000000002842, 0.000000000000000000, 0.000000000000000000 ) ) ;
#3947=AXIS2_PLACEMENT_3D ( 'NONE', #515, #4281, #3580 ) ;
#3951=FACE_BOUND ( 'NONE', #4354, .T. ) ;
#3960=FILL_AREA_STYLE ('',( #2440 ) ) ;
#3961=CARTESIAN_POINT ( 'NONE',  ( -31.74999999999995737, 3.061616997868384127E-16, -2.500000000000000888 ) ) ;
#3977=( NAMED_UNIT ( * ) PLANE_ANGLE_UNIT ( ) SI_UNIT ( $, .RADIAN. ) );
#3981=COLOUR_RGB ( '', 0.66274510, 0.83137255, 0.94901961) ;
#4002=CIRCLE ( 'NONE', #89, 2.041999999999999815 ) ;
#4012=SURFACE_STYLE_USAGE ( .BOTH. , #3712 ) ;
#4018=DIRECTION ( 'NONE',  ( -1.000000000000000000, -0.000000000000000000, -0.000000000000000000 ) ) ;
#4024=EDGE_CURVE ( 'NONE', #4850, #340, #829, .T. ) ;
#4029=ORIENTED_EDGE ( 'NONE', *, *, #3058, .F. ) ;
#4037=LINE ( 'NONE', #4347, #1129 ) ;
#4057=LINE ( 'NONE', #4079, #1621 ) ;
#4062=DIRECTION ( 'NONE',  ( 0.000000000000000000, 0.000000000000000000, 1.000000000000000000 ) ) ;
#4074=AXIS2_PLACEMENT_3D ( 'NONE', #4931, #346, #669 ) ;
#4079=CARTESIAN_POINT ( 'NONE',  ( 25.00000000000000000, 0.000000000000000000, 2.055000000000000160 ) ) ;
#4085=( NAMED_UNIT ( * ) SI_UNIT ( $, .STERADIAN. ) SOLID_ANGLE_UNIT ( ) );
#4099=VECTOR ( 'NONE', #2323, 1000.000000000000114 ) ;
#4100=CIRCLE ( 'NONE', #3233, 0.2000000000000000944 ) ;
#4123=CARTESIAN_POINT ( 'NONE',  ( 5.000000000000002665, 0.000000000000000000, -2.700000000000001066 ) ) ;
#4135=CARTESIAN_POINT ( 'NONE',  ( 5.200000000000002842, 3.306546357697854719E-16, 2.700000000000001066 ) ) ;
#4162=ORIENTED_EDGE ( 'NONE', *, *, #4704, .F. ) ;
#4176=AXIS2_PLACEMENT_3D ( 'NONE', #2136, #3240, #252 ) ;
#4177=CARTESIAN_POINT ( 'NONE',  ( 0.2500000000000002220, 0.000000000000000000, 4.250000000000000000 ) ) ;
#4179=CARTESIAN_POINT ( 'NONE',  ( 24.55500000000002103, 0.000000000000000000, 2.500000000000001332 ) ) ;
#4182=VERTEX_POINT ( 'NONE', #4772 ) ;
#4194=DIRECTION ( 'NONE',  ( -1.000000000000000000, -0.000000000000000000, -0.000000000000000000 ) ) ;
#4203=ORIENTED_EDGE ( 'NONE', *, *, #1903, .T. ) ;
#4210=ORIENTED_EDGE ( 'NONE', *, *, #3573, .T. ) ;
#4246=PRODUCT_DEFINITION_SHAPE ( 'NONE', 'NONE',  #2307 ) ;
#4247=CARTESIAN_POINT ( 'NONE',  ( 0.000000000000000000, -1.178949249685213863, 2.042000000000002924 ) ) ;
#4276=EDGE_CURVE ( 'NONE', #1179, #2929, #4057, .T. ) ;
#4281=DIRECTION ( 'NONE',  ( -1.000000000000000000, -0.000000000000000000, -0.000000000000000000 ) ) ;
#4289=ORIENTED_EDGE ( 'NONE', *, *, #3269, .F. ) ;
#4295=DIRECTION ( 'NONE',  ( 1.000000000000000000, 0.000000000000000000, 0.000000000000000000 ) ) ;
#4296=VERTEX_POINT ( 'NONE', #1807 ) ;
#4299=LINE ( 'NONE', #4778, #3203 ) ;
#4300=CARTESIAN_POINT ( 'NONE',  ( 2.500000000000000000, 2.357898499370433054, -1.951563910473907981E-15 ) ) ;
#4306=FACE_OUTER_BOUND ( 'NONE', #2914, .T. ) ;
#4320=DIRECTION ( 'NONE',  ( 0.000000000000000000, 0.000000000000000000, 1.000000000000000000 ) ) ;
#4330=CARTESIAN_POINT ( 'NONE',  ( 2.500000000000000000, 1.178949249685213863, -2.042000000000001148 ) ) ;
#4333=LINE ( 'NONE', #3961, #3155 ) ;
#4341=AXIS2_PLACEMENT_3D ( 'NONE', #3115, #1207, #3215 ) ;
#4347=CARTESIAN_POINT ( 'NONE',  ( 0.000000000000000000, 2.357898499370433054, -1.951563910473907981E-15 ) ) ;
#4351=VERTEX_POINT ( 'NONE', #605 ) ;
#4354=EDGE_LOOP ( 'NONE', ( #1218, #1422, #90, #1014, #3405, #36 ) ) ;
#4379=SURFACE_STYLE_FILL_AREA ( #3960 ) ;
#4392=ORIENTED_EDGE ( 'NONE', *, *, #3653, .T. ) ;
#4402=CIRCLE ( 'NONE', #1442, 2.055000000000000160 ) ;
#4406=VECTOR ( 'NONE', #52, 1000.000000000000000 ) ;
#4409=EDGE_CURVE ( 'NONE', #1320, #2431, #2665, .T. ) ;
#4411=EDGE_CURVE ( 'NONE', #1819, #1050, #2304, .T. ) ;
#4416=ORIENTED_EDGE ( 'NONE', *, *, #172, .T. ) ;
#4419=EDGE_CURVE ( 'NONE', #3852, #571, #404, .T. ) ;
#4433=DIRECTION ( 'NONE',  ( 0.000000000000000000, 0.000000000000000000, -1.000000000000000000 ) ) ;
#4444=ADVANCED_FACE ( 'NONE', ( #2336 ), #3861, .T. ) ;
#4445=PLANE ( 'NONE',  #2850 ) ;
#4456=FILL_AREA_STYLE_COLOUR ( '', #3981 ) ;
#4460=DIRECTION ( 'NONE',  ( -1.000000000000000000, -0.000000000000000000, -0.000000000000000000 ) ) ;
#4464=CARTESIAN_POINT ( 'NONE',  ( 5.200000000000002842, 0.000000000000000000, 2.500000000000000888 ) ) ;
#4477=DIRECTION ( 'NONE',  ( 0.000000000000000000, 0.000000000000000000, -1.000000000000000000 ) ) ;
#4486=ORIENTED_EDGE ( 'NONE', *, *, #2278, .T. ) ;
#4488=AXIS2_PLACEMENT_3D ( 'NONE', #3794, #1172, #3084 ) ;
#4493=ORIENTED_EDGE ( 'NONE', *, *, #3119, .T. ) ;
#4495=PLANE ( 'NONE',  #1874 ) ;
#4502=CARTESIAN_POINT ( 'NONE',  ( 2.500000000000000000, -2.357898499370432610, 3.252606517456513302E-15 ) ) ;
#4505=EDGE_CURVE ( 'NONE', #2974, #4182, #1073, .T. ) ;
#4517=ORIENTED_EDGE ( 'NONE', *, *, #2930, .F. ) ;
#4522=ORIENTED_EDGE ( 'NONE', *, *, #4609, .T. ) ;
#4536=ORIENTED_EDGE ( 'NONE', *, *, #4409, .T. ) ;
#4549=VECTOR ( 'NONE', #3500, 1000.000000000000000 ) ;
#4554=AXIS2_PLACEMENT_3D ( 'NONE', #1796, #3327, #1018 ) ;
#4568=VERTEX_POINT ( 'NONE', #4123 ) ;
#4585=FACE_OUTER_BOUND ( 'NONE', #2880, .T. ) ;
#4596=ORIENTED_EDGE ( 'NONE', *, *, #3475, .T. ) ;
#4600=EDGE_CURVE ( 'NONE', #1395, #115, #1097, .T. ) ;
#4609=EDGE_CURVE ( 'NONE', #3747, #1716, #1280, .T. ) ;
#4616=DIRECTION ( 'NONE',  ( 0.000000000000000000, -1.000000000000000000, 0.000000000000000000 ) ) ;
#4619=EDGE_LOOP ( 'NONE', ( #3427, #1332, #4203, #3561 ) ) ;
#4621=FACE_OUTER_BOUND ( 'NONE', #1346, .T. ) ;
#4643=FACE_OUTER_BOUND ( 'NONE', #3028, .T. ) ;
#4645=CARTESIAN_POINT ( 'NONE',  ( 2.500000000000000000, -1.178949249685213863, 2.042000000000002924 ) ) ;
#4684=CARTESIAN_POINT ( 'NONE',  ( 2.500000000000000000, 0.000000000000000000, 0.000000000000000000 ) ) ;
#4693=CARTESIAN_POINT ( 'NONE',  ( 2.500000000000000000, 2.357898499370433054, -1.951563910473907981E-15 ) ) ;
#4695=ORIENTED_EDGE ( 'NONE', *, *, #1333, .T. ) ;
#4698=EDGE_CURVE ( 'NONE', #216, #2709, #3480, .T. ) ;
#4699=DIRECTION ( 'NONE',  ( -0.5000000000000051070, 1.060575238724903217E-16, -0.8660254037844355990 ) ) ;
#4704=EDGE_CURVE ( 'NONE', #45, #645, #1514, .T. ) ;
#4719=DIRECTION ( 'NONE',  ( -1.000000000000000000, -0.000000000000000000, -0.000000000000000000 ) ) ;
#4720=CYLINDRICAL_SURFACE ( 'NONE', #1777, 4.250000000000000000 ) ;
#4724=EDGE_CURVE ( 'NONE', #1179, #3810, #2159, .T. ) ;
#4732=AXIS2_PLACEMENT_3D ( 'NONE', #2393, #57, #3122 ) ;
#4733=DIRECTION ( 'NONE',  ( -1.000000000000000000, -0.000000000000000000, -0.000000000000000000 ) ) ;
#4748=SHAPE_REPRESENTATION ( 'socket head cap screw_iso_ISO 4762 M5 x 20 - 20N', ( #1918 ), #3816 ) ;
#4751=DIRECTION ( 'NONE',  ( -1.000000000000000000, -0.000000000000000000, -0.000000000000000000 ) ) ;
#4764=DIRECTION ( 'NONE',  ( 0.000000000000000000, 0.000000000000000000, 1.000000000000000000 ) ) ;
#4765=ORIENTED_EDGE ( 'NONE', *, *, #4789, .F. ) ;
#4772=CARTESIAN_POINT ( 'NONE',  ( 0.000000000000000000, -2.357898499370432610, 3.252606517456513302E-15 ) ) ;
#4775=CARTESIAN_POINT ( 'NONE',  ( 5.200000000000002842, 3.061616997868384127E-16, -2.500000000000000888 ) ) ;
#4777=ORIENTED_EDGE ( 'NONE', *, *, #146, .F. ) ;
#4778=CARTESIAN_POINT ( 'NONE',  ( 2.500000000000000000, 2.500728763858895382E-16, -2.041999999999999815 ) ) ;
#4789=EDGE_CURVE ( 'NONE', #1819, #4296, #4299, .T. ) ;
#4793=SHAPE_REPRESENTATION_RELATIONSHIP ( 'NONE' , 'NONE' ,  #4748, #996 ) ;
#4795=DIRECTION ( 'NONE',  ( 0.000000000000000000, -1.224646799147353454E-16, 1.000000000000000000 ) ) ;
#4803=VECTOR ( 'NONE', #3501, 1000.000000000000000 ) ;
#4807=PLANE ( 'NONE',  #4176 ) ;
#4809=EDGE_LOOP ( 'NONE', ( #813, #2958 ) ) ;
#4825=EDGE_CURVE ( 'NONE', #2929, #4351, #3669, .T. ) ;
#4828=VECTOR ( 'NONE', #3896, 1000.000000000000000 ) ;
#4833=ORIENTED_EDGE ( 'NONE', *, *, #4698, .T. ) ;
#4850=VERTEX_POINT ( 'NONE', #315 ) ;
#4861=CARTESIAN_POINT ( 'NONE',  ( 3.678949249685231848, 0.000000000000000000, 0.000000000000000000 ) ) ;
#4867=( NAMED_UNIT ( * ) PLANE_ANGLE_UNIT ( ) SI_UNIT ( $, .RADIAN. ) );
#4869=LINE ( 'NONE', #2238, #332 ) ;
#4881=CARTESIAN_POINT ( 'NONE',  ( 2.500000000000000000, 2.357898499370433054, -1.951563910473907981E-15 ) ) ;
#4888=CARTESIAN_POINT ( 'NONE',  ( 2.500000000000000000, 0.000000000000000000, 0.000000000000000000 ) ) ;
#4890=ORIENTED_EDGE ( 'NONE', *, *, #1254, .T. ) ;
#4903=LINE ( 'NONE', #3371, #1437 ) ;
#4908=CARTESIAN_POINT ( 'NONE',  ( 5.000000000000002665, 3.306546357697854226E-16, 2.700000000000001066 ) ) ;
#4913=DIRECTION ( 'NONE',  ( 0.000000000000000000, -1.000000000000000000, 0.000000000000000000 ) ) ;
#4931=CARTESIAN_POINT ( 'NONE',  ( 24.55500000000002103, 0.000000000000000000, 0.000000000000000000 ) ) ;
#4941=DIRECTION ( 'NONE',  ( -1.000000000000000000, -0.000000000000000000, -0.000000000000000000 ) ) ;
#4954=FACE_OUTER_BOUND ( 'NONE', #736, .T. ) ;
#4957=DIRECTION ( 'NONE',  ( -1.000000000000000000, -0.000000000000000000, -0.000000000000000000 ) ) ;
ENDSEC;
END-ISO-10303-21;
